ISO-10303-21;
HEADER;
FILE_DESCRIPTION (('STEP AP214'),
    '1' );
FILE_NAME ('Pivot Pin.step',
    '2026-10-06T09:00:30',
    ( '' ),
    ( '' ),
    'SwSTEP 2.0',
    'SolidWorks 2020',
    '' );
FILE_SCHEMA (( 'AUTOMOTIVE_DESIGN' ));
ENDSEC;

DATA;
#11=CARTESIAN_POINT ( 'NONE',  ( 9.499999999614264112, -13.84939817494163350, -36.47165854346829406 ) ) ;
#172=ADVANCED_BREP_SHAPE_REPRESENTATION ( '', ( #20871, #17722 ), #24361 ) ;
#212=CIRCLE ( 'NONE', #1212, 2.299999999999999822 ) ;
#252=ORIENTED_EDGE ( 'NONE', *, *, #15221, .F. ) ;
#263=PRODUCT_DEFINITION_CONTEXT ( 'detailed design', #6356, 'design' ) ;
#321=EDGE_LOOP ( 'NONE', ( #8069, #252, #28865, #19891 ) ) ;
#341=CARTESIAN_POINT ( 'NONE',  ( 9.499999999713729437, -18.10015590263875396, -36.47860036342770229 ) ) ;
#389=ADVANCED_FACE ( 'NONE', ( #25945 ), #10756, .T. ) ;
#459=CARTESIAN_POINT ( 'NONE',  ( 9.799999999872998302, 8.682826176889994585, 14.90608581632256424 ) ) ;
#550=DIRECTION ( 'NONE',  ( -1.000000000000000000, 5.063197467948052462E-16, -2.257212216284997029E-12 ) ) ;
#567=EDGE_CURVE ( 'NONE', #6895, #23236, #6073, .T. ) ;
#656=( NAMED_UNIT ( * ) PLANE_ANGLE_UNIT ( ) SI_UNIT ( $, .RADIAN. ) );
#793=CARTESIAN_POINT ( 'NONE',  ( -9.700000000002093614, -15.94902145826220696, -35.53273252502236090 ) ) ;
#808=SURFACE_SIDE_STYLE ('',( #24564 ) ) ;
#925=AXIS2_PLACEMENT_3D ( 'NONE', #19192, #16825, #15877 ) ;
#962=CARTESIAN_POINT ( 'NONE',  ( 9.499999999998065547, -18.19953924290990344, -36.00725302081955448 ) ) ;
#1010=ORIENTED_EDGE ( 'NONE', *, *, #19425, .F. ) ;
#1087=ORIENTED_EDGE ( 'NONE', *, *, #23894, .T. ) ;
#1147=VECTOR ( 'NONE', #1778, 1000.000000000000114 ) ;
#1212=AXIS2_PLACEMENT_3D ( 'NONE', #26161, #16699, #18916 ) ;
#1225=EDGE_CURVE ( 'NONE', #7840, #24939, #24789, .T. ) ;
#1485=( LENGTH_UNIT ( ) NAMED_UNIT ( * ) SI_UNIT ( .MILLI., .METRE. ) );
#1600=ORIENTED_EDGE ( 'NONE', *, *, #17500, .F. ) ;
#1778=DIRECTION ( 'NONE',  ( -0.7071067811869131692, -0.6918940811759506371, -0.1458855045341028167 ) ) ;
#1874=CARTESIAN_POINT ( 'NONE',  ( 10.80000000000790550, -15.94902145823651907, -35.53273252494266643 ) ) ;
#2123=LINE ( 'NONE', #25895, #3671 ) ;
#2188=DIRECTION ( 'NONE',  ( -1.000000000000000000, -1.433034374054745923E-13, -1.199006074477166028E-12 ) ) ;
#2192=AXIS2_PLACEMENT_3D ( 'NONE', #7627, #22265, #12194 ) ;
#2248=VERTEX_POINT ( 'NONE', #11694 ) ;
#2360=CARTESIAN_POINT ( 'NONE',  ( 9.499999999611546286, -18.04864474152872589, -34.59380650643552713 ) ) ;
#2453=DIRECTION ( 'NONE',  ( 3.590123367689346428E-13, 0.9128796883888948832, -0.4082287037029536658 ) ) ;
#2474=AXIS2_PLACEMENT_3D ( 'NONE', #5283, #7335, #24478 ) ;
#2484=VECTOR ( 'NONE', #18932, 1000.000000000000000 ) ;
#2527=VERTEX_POINT ( 'NONE', #11771 ) ;
#2531=ADVANCED_FACE ( 'NONE', ( #29917 ), #30167, .T. ) ;
#2627=CARTESIAN_POINT ( 'NONE',  ( 0.000000000000000000, 0.000000000000000000, 0.000000000000000000 ) ) ;
#2783=FACE_OUTER_BOUND ( 'NONE', #321, .T. ) ;
#2915=FACE_OUTER_BOUND ( 'NONE', #29872, .T. ) ;
#2919=AXIS2_PLACEMENT_3D ( 'NONE', #27908, #26020, #23666 ) ;
#3061=ORIENTED_EDGE ( 'NONE', *, *, #15221, .T. ) ;
#3136=EDGE_CURVE ( 'NONE', #7840, #28202, #19405, .T. ) ;
#3239=CARTESIAN_POINT ( 'NONE',  ( 9.799999999993435296, -14.12326182050966139, -36.34918934884738206 ) ) ;
#3345=CYLINDRICAL_SURFACE ( 'NONE', #8263, 2.299999999999999822 ) ;
#3359=AXIS2_PLACEMENT_3D ( 'NONE', #4958, #12652, #2453 ) ;
#3452=CARTESIAN_POINT ( 'NONE',  ( 9.499999999662559702, -18.29892258314324494, -35.53590567821694890 ) ) ;
#3526=PRODUCT ( 'Pivot Pin', 'Pivot Pin', '', ( #20272 ) ) ;
#3671=VECTOR ( 'NONE', #21163, 1000.000000000000114 ) ;
#3832=ADVANCED_FACE ( 'NONE', ( #4856 ), #17943, .T. ) ;
#4035=CARTESIAN_POINT ( 'NONE',  ( -10.00000000001209344, -15.94902145808038618, -35.53273252466679111 ) ) ;
#4147=SHAPE_REPRESENTATION_RELATIONSHIP ( 'NONE' , 'NONE' ,  #28252, #172 ) ;
#4213=ORIENTED_EDGE ( 'NONE', *, *, #30162, .F. ) ;
#4215=VECTOR ( 'NONE', #8723, 1000.000000000000000 ) ;
#4436=AXIS2_PLACEMENT_3D ( 'NONE', #793, #12274, #10383 ) ;
#4568=ORIENTED_EDGE ( 'NONE', *, *, #9104, .F. ) ;
#4730=ORIENTED_EDGE ( 'NONE', *, *, #567, .T. ) ;
#4856=FACE_OUTER_BOUND ( 'NONE', #19999, .T. ) ;
#4861=CARTESIAN_POINT ( 'NONE',  ( -9.699999999996551381, -18.19238022167704116, -35.02544418635115875 ) ) ;
#4895=CARTESIAN_POINT ( 'NONE',  ( 9.499999999614264112, -13.84939817494163350, -36.47165854346829406 ) ) ;
#4958=CARTESIAN_POINT ( 'NONE',  ( -9.700000000002093614, -15.94902145825307826, -35.53273252502644652 ) ) ;
#5068=ORIENTED_EDGE ( 'NONE', *, *, #15083, .F. ) ;
#5090=DIRECTION ( 'NONE',  ( -9.220055274816719609E-13, -0.9128796883888953273, 0.4082287037029531662 ) ) ;
#5102=COLOUR_RGB ( '', 0.66274510, 0.83137255, 0.94901961) ;
#5283=CARTESIAN_POINT ( 'NONE',  ( -10.99999999999209344, -15.94902145825930617, -35.53273252503056767 ) ) ;
#5284=EDGE_LOOP ( 'NONE', ( #4730, #3061, #16118, #7392 ) ) ;
#5360=FILL_AREA_STYLE ('',( #26924 ) ) ;
#5515=DIRECTION ( 'NONE',  ( -1.000000000000000000, -1.433034374091448024E-13, -1.199006074478416896E-12 ) ) ;
#5636=ORIENTED_EDGE ( 'NONE', *, *, #31002, .F. ) ;
#5779=CARTESIAN_POINT ( 'NONE',  ( 9.799999999997906386, -15.94902145823454198, -35.53273252495090873 ) ) ;
#5908=EDGE_LOOP ( 'NONE', ( #6312, #25168, #14333, #14844 ) ) ;
#5971=( LENGTH_UNIT ( ) NAMED_UNIT ( * ) SI_UNIT ( .MILLI., .METRE. ) );
#5995=DIRECTION ( 'NONE',  ( -3.868433351431744750E-13, 0.9784859933254772546, 0.2063132590645932463 ) ) ;
#6073=LINE ( 'NONE', #27173, #13682 ) ;
#6229=ORIENTED_EDGE ( 'NONE', *, *, #17891, .F. ) ;
#6312=ORIENTED_EDGE ( 'NONE', *, *, #17697, .T. ) ;
#6356=APPLICATION_CONTEXT ( 'automotive_design' ) ;
#6502=SURFACE_SIDE_STYLE ('',( #18139 ) ) ;
#6688=AXIS2_PLACEMENT_3D ( 'NONE', #30384, #15736, #8969 ) ;
#6754=CIRCLE ( 'NONE', #25334, 2.000000000000002220 ) ;
#6891=FACE_OUTER_BOUND ( 'NONE', #10836, .T. ) ;
#6895=VERTEX_POINT ( 'NONE', #14796 ) ;
#6973=B_SPLINE_CURVE_WITH_KNOTS ( 'NONE', 3,
 ( #962, #3452, #24565, #22201 ),
 .UNSPECIFIED., .F., .F.,
 ( 4, 4 ),
 ( 0.000000000000000000, 1.000000000000000000 ),
 .UNSPECIFIED. ) ;
#7021=EDGE_CURVE ( 'NONE', #2527, #6895, #9028, .T. ) ;
#7335=DIRECTION ( 'NONE',  ( 1.000000000000000000, 7.807837518093016606E-13, 2.626330150305131362E-12 ) ) ;
#7392=ORIENTED_EDGE ( 'NONE', *, *, #21231, .F. ) ;
#7444=EDGE_LOOP ( 'NONE', ( #20422, #16741, #20938, #23854 ) ) ;
#7627=CARTESIAN_POINT ( 'NONE',  ( 10.80000000000790550, -15.94902145823636985, -35.53273252494371093 ) ) ;
#7782=UNCERTAINTY_MEASURE_WITH_UNIT (LENGTH_MEASURE( 1.000000000000000082E-05 ), #1485, 'distance_accuracy_value', 'NONE');
#7840=VERTEX_POINT ( 'NONE', #22389 ) ;
#7964=EDGE_CURVE ( 'NONE', #7840, #8976, #16877, .T. ) ;
#8069=ORIENTED_EDGE ( 'NONE', *, *, #3136, .T. ) ;
#8263=AXIS2_PLACEMENT_3D ( 'NONE', #15318, #24919, #15936 ) ;
#8281=ADVANCED_FACE ( 'NONE', ( #6891 ), #30977, .F. ) ;
#8342=CARTESIAN_POINT ( 'NONE',  ( 10.80000000000790550, -15.94902145823651907, -35.53273252494266643 ) ) ;
#8438=DIRECTION ( 'NONE',  ( -1.000000000000000000, 5.063197467948052462E-16, -2.257212216284997029E-12 ) ) ;
#8539=PRESENTATION_STYLE_ASSIGNMENT (( #8694 ) ) ;
#8660=CIRCLE ( 'NONE', #12682, 2.000000000000002220 ) ;
#8694=SURFACE_STYLE_USAGE ( .BOTH. , #6502 ) ;
#8723=DIRECTION ( 'NONE',  ( -1.000000000000000000, 5.063197998645201881E-16, -2.257212216166322864E-12 ) ) ;
#8736=DIRECTION ( 'NONE',  ( -1.000000000000000000, -7.807837518030243978E-13, -2.626330150303133688E-12 ) ) ;
#8782=( GEOMETRIC_REPRESENTATION_CONTEXT ( 3 ) GLOBAL_UNCERTAINTY_ASSIGNED_CONTEXT ( ( #9686 ) ) GLOBAL_UNIT_ASSIGNED_CONTEXT ( ( #23356, #27741, #13588 ) ) REPRESENTATION_CONTEXT ( 'NONE', 'WORKASPACE' ) );
#8894=DIRECTION ( 'NONE',  ( 3.590123367689346428E-13, 0.9128796883888948832, -0.4082287037029536658 ) ) ;
#8969=DIRECTION ( 'NONE',  ( -9.228728892150466515E-13, -0.9128796883888956604, 0.4082287037029523336 ) ) ;
#8976=VERTEX_POINT ( 'NONE', #10491 ) ;
#9015=( NAMED_UNIT ( * ) PLANE_ANGLE_UNIT ( ) SI_UNIT ( $, .RADIAN. ) );
#9028=CIRCLE ( 'NONE', #27618, 2.000000000000002220 ) ;
#9104=EDGE_CURVE ( 'NONE', #15917, #23236, #21507, .T. ) ;
#9328=PRODUCT_DEFINITION_FORMATION_WITH_SPECIFIED_SOURCE ( 'ANY', '', #3526, .NOT_KNOWN. ) ;
#9508=ADVANCED_FACE ( 'NONE', ( #16413 ), #30270, .T. ) ;
#9607=DIRECTION ( 'NONE',  ( 0.7071067811870024311, 0.6455034180679679601, -0.2886612846606330662 ) ) ;
#9686=UNCERTAINTY_MEASURE_WITH_UNIT (LENGTH_MEASURE( 1.000000000000000082E-05 ), #23356, 'distance_accuracy_value', 'NONE');
#9742=EDGE_LOOP ( 'NONE', ( #30921, #10005, #10185, #4213 ) ) ;
#9808=MECHANICAL_DESIGN_GEOMETRIC_PRESENTATION_REPRESENTATION('',(#12814),#8782);
#10005=ORIENTED_EDGE ( 'NONE', *, *, #31002, .T. ) ;
#10185=ORIENTED_EDGE ( 'NONE', *, *, #1225, .F. ) ;
#10355=EDGE_CURVE ( 'NONE', #28202, #15917, #22961, .T. ) ;
#10383=DIRECTION ( 'NONE',  ( 1.485828368566968728E-12, 0.9128796883888956604, -0.4082287037029520560 ) ) ;
#10487=ORIENTED_EDGE ( 'NONE', *, *, #10355, .F. ) ;
#10491=CARTESIAN_POINT ( 'NONE',  ( 9.499999999998065547, -18.19953924290990344, -36.00725302081955448 ) ) ;
#10756=CONICAL_SURFACE ( 'NONE', #25846, 0.9999999999991018296, 0.7853981633970000820 ) ;
#10836=EDGE_LOOP ( 'NONE', ( #5636, #6229, #11183 ) ) ;
#11047=FACE_OUTER_BOUND ( 'NONE', #30851, .T. ) ;
#11085=AXIS2_PLACEMENT_3D ( 'NONE', #8342, #17938, #5995 ) ;
#11183=ORIENTED_EDGE ( 'NONE', *, *, #18852, .F. ) ;
#11473=DIRECTION ( 'NONE',  ( 3.868433351431744750E-13, -0.9784859933254772546, -0.2063132590645932463 ) ) ;
#11566=ADVANCED_FACE ( 'NONE', ( #23929 ), #12971, .T. ) ;
#11618=DIRECTION ( 'NONE',  ( -1.821459649777283484E-13, 0.9753733754015535551, -0.2205601472564346632 ) ) ;
#11694=CARTESIAN_POINT ( 'NONE',  ( 9.799999999982377474, -17.77478083483991966, -34.71627511718394032 ) ) ;
#11771=CARTESIAN_POINT ( 'NONE',  ( -10.00000000001596767, -17.89976820896369247, -35.09161223051660983 ) ) ;
#11803=COLOUR_RGB ( '', 0.66274510, 0.83137255, 0.94901961) ;
#12103=CARTESIAN_POINT ( 'NONE',  ( 9.599999999813990215, -13.94068574325910426, -36.43083477791316227 ) ) ;
#12194=DIRECTION ( 'NONE',  ( -9.228728892204885548E-13, -0.9128796883888958824, 0.4082287037029517784 ) ) ;
#12267=ORIENTED_EDGE ( 'NONE', *, *, #10355, .T. ) ;
#12274=DIRECTION ( 'NONE',  ( -1.000000000000000000, 8.856532914347465582E-13, -1.659169102000414711E-12 ) ) ;
#12277=CARTESIAN_POINT ( 'NONE',  ( 9.499999999936914463, -14.38471058642483769, -37.28629371922507119 ) ) ;
#12652=DIRECTION ( 'NONE',  ( -1.000000000000000000, -7.807837518030243978E-13, -2.626330150303133688E-12 ) ) ;
#12682=AXIS2_PLACEMENT_3D ( 'NONE', #17198, #550, #5090 ) ;
#12740=DIRECTION ( 'NONE',  ( 0.7071067811868604336, -0.6896931279344806764, 0.1559595757865139820 ) ) ;
#12814=STYLED_ITEM ( 'NONE', ( #8539 ), #172 ) ;
#12916=VERTEX_POINT ( 'NONE', #25452 ) ;
#12971=CONICAL_SURFACE ( 'NONE', #925, 0.9999999999991020516, 0.7853981633970000820 ) ;
#13017=DIRECTION ( 'NONE',  ( -9.220055274816719609E-13, -0.9128796883888953273, 0.4082287037029531662 ) ) ;
#13201=SURFACE_STYLE_USAGE ( .BOTH. , #808 ) ;
#13331=ADVANCED_FACE ( 'NONE', ( #2915 ), #23072, .T. ) ;
#13588=( NAMED_UNIT ( * ) SI_UNIT ( $, .STERADIAN. ) SOLID_ANGLE_UNIT ( ) );
#13632=DIRECTION ( 'NONE',  ( -9.220055274816719609E-13, -0.9128796883888953273, 0.4082287037029531662 ) ) ;
#13682=VECTOR ( 'NONE', #22760, 1000.000000000000227 ) ;
#13938=AXIS2_PLACEMENT_3D ( 'NONE', #459, #14458, #16494 ) ;
#14015=DIRECTION ( 'NONE',  ( 0.000000000000000000, 0.000000000000000000, 1.000000000000000000 ) ) ;
#14328=CARTESIAN_POINT ( 'NONE',  ( -10.00000000000656186, -14.12326208130076921, -36.34918993207352145 ) ) ;
#14333=ORIENTED_EDGE ( 'NONE', *, *, #1225, .T. ) ;
#14336=ORIENTED_EDGE ( 'NONE', *, *, #17500, .T. ) ;
#14347=CARTESIAN_POINT ( 'NONE',  ( 9.499999999998065547, -18.19953924290990344, -36.00725302081955448 ) ) ;
#14398=ORIENTED_EDGE ( 'NONE', *, *, #7964, .T. ) ;
#14458=DIRECTION ( 'NONE',  ( -1.000000000000000000, 5.063197467949062204E-16, -2.257212216284997029E-12 ) ) ;
#14796=CARTESIAN_POINT ( 'NONE',  ( -10.00000000001762146, -17.77478083485818061, -34.71627511726088500 ) ) ;
#14844=ORIENTED_EDGE ( 'NONE', *, *, #18852, .T. ) ;
#14955=CARTESIAN_POINT ( 'NONE',  ( 9.499999999888803615, -15.21984422747265420, -37.76664074417031713 ) ) ;
#15034=UNCERTAINTY_MEASURE_WITH_UNIT (LENGTH_MEASURE( 1.000000000000000082E-05 ), #5971, 'distance_accuracy_value', 'NONE');
#15075=DIRECTION ( 'NONE',  ( -3.582203977874193828E-13, -0.9128796883888956604, 0.4082287037029523336 ) ) ;
#15083=EDGE_CURVE ( 'NONE', #18133, #2248, #23477, .T. ) ;
#15118=DIRECTION ( 'NONE',  ( -3.582203977874193828E-13, -0.9128796883888956604, 0.4082287037029523336 ) ) ;
#15221=EDGE_CURVE ( 'NONE', #23236, #28202, #26538, .T. ) ;
#15225=CIRCLE ( 'NONE', #28300, 2.000000000010000889 ) ;
#15247=DIRECTION ( 'NONE',  ( -1.000000000000000000, 5.063197467948052462E-16, -2.257212216284997029E-12 ) ) ;
#15318=CARTESIAN_POINT ( 'NONE',  ( -0.1000000000151932966, -15.94902145824367246, -35.53273252498938461 ) ) ;
#15349=CARTESIAN_POINT ( 'NONE',  ( -0.1000000000709524162, -18.04864474153813347, -34.59380650647258904 ) ) ;
#15411=CARTESIAN_POINT ( 'NONE',  ( 353541.3905933150672, -344862.5129886576324, 77944.25516062910901 ) ) ;
#15526=EDGE_CURVE ( 'NONE', #2527, #15917, #19251, .T. ) ;
#15720=( NAMED_UNIT ( * ) SI_UNIT ( $, .STERADIAN. ) SOLID_ANGLE_UNIT ( ) );
#15736=DIRECTION ( 'NONE',  ( -1.000000000000000000, 4.717926049406357368E-15, -2.251139438558545733E-12 ) ) ;
#15877=DIRECTION ( 'NONE',  ( 1.486658018913458559E-12, 0.9128796883888955493, -0.4082287037029524446 ) ) ;
#15917=VERTEX_POINT ( 'NONE', #4861 ) ;
#15936=DIRECTION ( 'NONE',  ( -9.219194983962475343E-13, -0.9128796883888954383, 0.4082287037029530552 ) ) ;
#16118=ORIENTED_EDGE ( 'NONE', *, *, #28773, .F. ) ;
#16157=MECHANICAL_DESIGN_GEOMETRIC_PRESENTATION_REPRESENTATION('',(#25184),#27689);
#16240=CONICAL_SURFACE ( 'NONE', #2192, 0.9999999999991036059, 0.7853981633970000820 ) ;
#16251=FILL_AREA_STYLE_COLOUR ( '', #11803 ) ;
#16382=DIRECTION ( 'NONE',  ( 9.219194983962475343E-13, 0.9128796883888954383, -0.4082287037029530552 ) ) ;
#16413=FACE_OUTER_BOUND ( 'NONE', #25193, .T. ) ;
#16494=DIRECTION ( 'NONE',  ( 9.219210260491733511E-13, 0.9128796883888953273, -0.4082287037029530552 ) ) ;
#16662=AXIS2_PLACEMENT_3D ( 'NONE', #5779, #27032, #15075 ) ;
#16699=DIRECTION ( 'NONE',  ( -1.000000000000000000, 5.063197467948052462E-16, -2.257212216284997029E-12 ) ) ;
#16741=ORIENTED_EDGE ( 'NONE', *, *, #9104, .T. ) ;
#16825=DIRECTION ( 'NONE',  ( 1.000000000000000000, -8.856532914347465582E-13, 1.659169102000414711E-12 ) ) ;
#16845=CARTESIAN_POINT ( 'NONE',  ( 9.499999999739312528, -17.84826627069900340, -36.91653688543832601 ) ) ;
#16877=B_SPLINE_CURVE_WITH_KNOTS ( 'NONE', 3,
 ( #4895, #19369, #12277, #14955, #29260, #19677, #31014, #16845, #341, #14347 ),
 .UNSPECIFIED., .F., .F.,
 ( 4, 2, 2, 2, 4 ),
 ( 0.000000000000000000, 0.2500000000000000000, 0.5000000000000000000, 0.7500000000000000000, 1.000000000000000000 ),
 .UNSPECIFIED. ) ;
#16917=FACE_OUTER_BOUND ( 'NONE', #9742, .T. ) ;
#17015=APPLICATION_CONTEXT ( 'automotive_design' ) ;
#17198=CARTESIAN_POINT ( 'NONE',  ( -10.00000000001209344, -15.94902145808038618, -35.53273252466679111 ) ) ;
#17500=EDGE_CURVE ( 'NONE', #23358, #2527, #8660, .T. ) ;
#17615=PRESENTATION_STYLE_ASSIGNMENT (( #13201 ) ) ;
#17697=EDGE_CURVE ( 'NONE', #12916, #8976, #28352, .T. ) ;
#17722=AXIS2_PLACEMENT_3D ( 'NONE', #2627, #14015, #29203 ) ;
#17880=CARTESIAN_POINT ( 'NONE',  ( -10.00000000001209344, -15.94902145808038618, -35.53273252466679111 ) ) ;
#17891=EDGE_CURVE ( 'NONE', #12916, #2248, #15225, .T. ) ;
#17897=SHAPE_DEFINITION_REPRESENTATION ( #27648, #28252 ) ;
#17938=DIRECTION ( 'NONE',  ( -1.000000000000000000, -1.433034374054745923E-13, -1.199006074477166028E-12 ) ) ;
#17943=CONICAL_SURFACE ( 'NONE', #28526, 0.9999999999991042721, 0.7853981633970000820 ) ;
#18087=CARTESIAN_POINT ( 'NONE',  ( -9.699999999998452083, -18.04864474153841059, -34.59380650651372946 ) ) ;
#18133=VERTEX_POINT ( 'NONE', #2360 ) ;
#18139=SURFACE_STYLE_FILL_AREA ( #28211 ) ;
#18387=CARTESIAN_POINT ( 'NONE',  ( -10.99999999999209344, -15.94902145825930617, -35.53273252503056767 ) ) ;
#18399=ADVANCED_FACE ( 'NONE', ( #16917 ), #16240, .T. ) ;
#18428=CARTESIAN_POINT ( 'NONE',  ( -0.1000000000151932966, -15.94902145824367246, -35.53273252498938461 ) ) ;
#18499=CARTESIAN_POINT ( 'NONE',  ( -9.700000000002093614, -15.94902145825307826, -35.53273252502644652 ) ) ;
#18583=CLOSED_SHELL ( 'NONE', ( #8281, #18399, #3832, #2531, #25465, #20410, #11566, #389, #13331, #9508 ) ) ;
#18766=( NAMED_UNIT ( * ) SI_UNIT ( $, .STERADIAN. ) SOLID_ANGLE_UNIT ( ) );
#18852=EDGE_CURVE ( 'NONE', #24939, #12916, #29218, .T. ) ;
#18916=DIRECTION ( 'NONE',  ( -9.216661250624602488E-13, -0.9128796883888954383, 0.4082287037029530552 ) ) ;
#18932=DIRECTION ( 'NONE',  ( -1.000000000000000000, 5.063197998645201881E-16, -2.257212216166322864E-12 ) ) ;
#19192=CARTESIAN_POINT ( 'NONE',  ( -10.99999999999209344, -15.94902145826098483, -35.53273252503156243 ) ) ;
#19251=LINE ( 'NONE', #15411, #28060 ) ;
#19369=CARTESIAN_POINT ( 'NONE',  ( 9.499999999960662578, -14.04604638041797138, -36.91140261562396319 ) ) ;
#19405=LINE ( 'NONE', #23978, #2484 ) ;
#19425=EDGE_CURVE ( 'NONE', #8976, #18133, #6973, .T. ) ;
#19677=CARTESIAN_POINT ( 'NONE',  ( 9.499999999815022633, -16.67216299285837522, -37.76860186073199799 ) ) ;
#19891=ORIENTED_EDGE ( 'NONE', *, *, #30162, .T. ) ;
#19999=EDGE_LOOP ( 'NONE', ( #21883, #22376, #5068, #1010 ) ) ;
#20034=ORIENTED_EDGE ( 'NONE', *, *, #21231, .T. ) ;
#20272=PRODUCT_CONTEXT ( 'NONE', #17015, 'mechanical' ) ;
#20410=ADVANCED_FACE ( 'NONE', ( #11047 ), #25685, .T. ) ;
#20422=ORIENTED_EDGE ( 'NONE', *, *, #15526, .T. ) ;
#20871=MANIFOLD_SOLID_BREP ( 'PartBody', #18583 ) ;
#20938=ORIENTED_EDGE ( 'NONE', *, *, #567, .F. ) ;
#21163=DIRECTION ( 'NONE',  ( 0.7071067811870024311, 0.6455034179958023532, -0.2886612848220092009 ) ) ;
#21231=EDGE_CURVE ( 'NONE', #6895, #23358, #6754, .T. ) ;
#21410=ORIENTED_EDGE ( 'NONE', *, *, #28773, .T. ) ;
#21507=CIRCLE ( 'NONE', #25530, 2.299999999990001598 ) ;
#21883=ORIENTED_EDGE ( 'NONE', *, *, #17697, .F. ) ;
#22158=AXIS2_PLACEMENT_3D ( 'NONE', #18428, #27874, #16382 ) ;
#22201=CARTESIAN_POINT ( 'NONE',  ( 9.499999999611546286, -18.04864474152872589, -34.59380650643552713 ) ) ;
#22265=DIRECTION ( 'NONE',  ( -1.000000000000000000, 4.717926049406357368E-15, -2.251139438558545733E-12 ) ) ;
#22376=ORIENTED_EDGE ( 'NONE', *, *, #17891, .T. ) ;
#22389=CARTESIAN_POINT ( 'NONE',  ( 9.499999999614264112, -13.84939817494163350, -36.47165854346829406 ) ) ;
#22520=VECTOR ( 'NONE', #9607, 999.9999999999997726 ) ;
#22760=DIRECTION ( 'NONE',  ( 0.7071067811865924257, -0.6455034180660765841, 0.2886612846658665466 ) ) ;
#22961=CIRCLE ( 'NONE', #3359, 2.299999999990001598 ) ;
#23072=CONICAL_SURFACE ( 'NONE', #2474, 0.9999999999991018296, 0.7853981633970000820 ) ;
#23236=VERTEX_POINT ( 'NONE', #18087 ) ;
#23356=( LENGTH_UNIT ( ) NAMED_UNIT ( * ) SI_UNIT ( .MILLI., .METRE. ) );
#23358=VERTEX_POINT ( 'NONE', #14328 ) ;
#23477=LINE ( 'NONE', #30858, #22520 ) ;
#23594=DIRECTION ( 'NONE',  ( 1.000000000000000000, 7.807837518093016606E-13, 2.626330150305131362E-12 ) ) ;
#23666=DIRECTION ( 'NONE',  ( 9.219210260491733511E-13, 0.9128796883888953273, -0.4082287037029530552 ) ) ;
#23854=ORIENTED_EDGE ( 'NONE', *, *, #7021, .F. ) ;
#23894=EDGE_CURVE ( 'NONE', #18133, #23236, #29971, .T. ) ;
#23929=FACE_OUTER_BOUND ( 'NONE', #5284, .T. ) ;
#23978=CARTESIAN_POINT ( 'NONE',  ( -0.1000000000582341592, -13.84939817494921321, -36.47165854350617309 ) ) ;
#24167=ORIENTED_EDGE ( 'NONE', *, *, #15526, .F. ) ;
#24361=( GEOMETRIC_REPRESENTATION_CONTEXT ( 3 ) GLOBAL_UNCERTAINTY_ASSIGNED_CONTEXT ( ( #7782 ) ) GLOBAL_UNIT_ASSIGNED_CONTEXT ( ( #1485, #9015, #18766 ) ) REPRESENTATION_CONTEXT ( 'NONE', 'WORKASPACE' ) );
#24478=DIRECTION ( 'NONE',  ( 1.821459649777283484E-13, -0.9753733754015535551, 0.2205601472564346632 ) ) ;
#24564=SURFACE_STYLE_FILL_AREA ( #5360 ) ;
#24565=CARTESIAN_POINT ( 'NONE',  ( 9.499999999636983716, -18.24529294700720783, -35.03355057858191657 ) ) ;
#24789=B_SPLINE_CURVE_WITH_KNOTS ( 'NONE', 3,
 ( #11, #12103, #27165, #3239 ),
 .UNSPECIFIED., .F., .F.,
 ( 4, 4 ),
 ( -0.5999999999999999778, 0.000000000000000000 ),
 .UNSPECIFIED. ) ;
#24919=DIRECTION ( 'NONE',  ( -1.000000000000000000, 5.063197467948052462E-16, -2.257212216284997029E-12 ) ) ;
#24939=VERTEX_POINT ( 'NONE', #25663 ) ;
#25036=ORIENTED_EDGE ( 'NONE', *, *, #7021, .T. ) ;
#25168=ORIENTED_EDGE ( 'NONE', *, *, #7964, .F. ) ;
#25184=STYLED_ITEM ( 'NONE', ( #17615 ), #20871 ) ;
#25193=EDGE_LOOP ( 'NONE', ( #14336, #25036, #20034 ) ) ;
#25334=AXIS2_PLACEMENT_3D ( 'NONE', #17880, #8438, #13017 ) ;
#25452=CARTESIAN_POINT ( 'NONE',  ( 9.799999999988044053, -17.90599344469555732, -35.94535904307270613 ) ) ;
#25465=ADVANCED_FACE ( 'NONE', ( #2783 ), #3345, .T. ) ;
#25530=AXIS2_PLACEMENT_3D ( 'NONE', #18499, #8736, #8894 ) ;
#25663=CARTESIAN_POINT ( 'NONE',  ( 9.799999999993435296, -14.12326182050966139, -36.34918934884738206 ) ) ;
#25685=CYLINDRICAL_SURFACE ( 'NONE', #22158, 2.299999999999999822 ) ;
#25797=CIRCLE ( 'NONE', #6688, 2.000000000010000889 ) ;
#25846=AXIS2_PLACEMENT_3D ( 'NONE', #18387, #23594, #11618 ) ;
#25895=CARTESIAN_POINT ( 'NONE',  ( 353541.3905939778197, 322735.7599763900507, -144366.1751435059414 ) ) ;
#25945=FACE_OUTER_BOUND ( 'NONE', #7444, .T. ) ;
#26020=DIRECTION ( 'NONE',  ( -1.000000000000000000, 5.063197467949062204E-16, -2.257212216284997029E-12 ) ) ;
#26161=CARTESIAN_POINT ( 'NONE',  ( 9.499999999607904755, -15.94902145823426665, -35.53273252495232271 ) ) ;
#26538=CIRCLE ( 'NONE', #4436, 2.299999999979998933 ) ;
#26924=FILL_AREA_STYLE_COLOUR ( '', #5102 ) ;
#26933=PRODUCT_DEFINITION ( 'UNKNOWN', '', #9328, #263 ) ;
#27032=DIRECTION ( 'NONE',  ( -1.000000000000000000, -1.433034374091448024E-13, -1.199006074478416896E-12 ) ) ;
#27077=CARTESIAN_POINT ( 'NONE',  ( 9.799999999997906386, -15.94902145823454198, -35.53273252495090873 ) ) ;
#27165=CARTESIAN_POINT ( 'NONE',  ( 9.700000000183711890, -14.03197393871519516, -36.39001241340137938 ) ) ;
#27173=CARTESIAN_POINT ( 'NONE',  ( 353541.3905930228066, -322767.6580542778247, 144295.1096003104758 ) ) ;
#27618=AXIS2_PLACEMENT_3D ( 'NONE', #4035, #15247, #13632 ) ;
#27648=PRODUCT_DEFINITION_SHAPE ( 'NONE', 'NONE',  #26933 ) ;
#27689=( GEOMETRIC_REPRESENTATION_CONTEXT ( 3 ) GLOBAL_UNCERTAINTY_ASSIGNED_CONTEXT ( ( #15034 ) ) GLOBAL_UNIT_ASSIGNED_CONTEXT ( ( #5971, #656, #15720 ) ) REPRESENTATION_CONTEXT ( 'NONE', 'WORKASPACE' ) );
#27741=( NAMED_UNIT ( * ) PLANE_ANGLE_UNIT ( ) SI_UNIT ( $, .RADIAN. ) );
#27874=DIRECTION ( 'NONE',  ( -1.000000000000000000, 5.063197467948052462E-16, -2.257212216284997029E-12 ) ) ;
#27908=CARTESIAN_POINT ( 'NONE',  ( -10.00000000012699886, 8.682826176890005243, 14.90608581627787110 ) ) ;
#28060=VECTOR ( 'NONE', #12740, 1000.000000000000227 ) ;
#28202=VERTEX_POINT ( 'NONE', #29931 ) ;
#28211=FILL_AREA_STYLE ('',( #16251 ) ) ;
#28252=SHAPE_REPRESENTATION ( 'Pivot Pin', ( #17722 ), #24361 ) ;
#28300=AXIS2_PLACEMENT_3D ( 'NONE', #27077, #5515, #15118 ) ;
#28352=LINE ( 'NONE', #30878, #1147 ) ;
#28526=AXIS2_PLACEMENT_3D ( 'NONE', #1874, #2188, #11473 ) ;
#28773=EDGE_CURVE ( 'NONE', #23358, #28202, #2123, .T. ) ;
#28829=ORIENTED_EDGE ( 'NONE', *, *, #3136, .F. ) ;
#28865=ORIENTED_EDGE ( 'NONE', *, *, #23894, .F. ) ;
#29203=DIRECTION ( 'NONE',  ( 1.000000000000000000, 0.000000000000000000, 0.000000000000000000 ) ) ;
#29218=CIRCLE ( 'NONE', #16662, 2.000000000010000889 ) ;
#29260=CARTESIAN_POINT ( 'NONE',  ( 9.499999999864446210, -15.71418478743095548, -37.87087219225396950 ) ) ;
#29325=ORIENTED_EDGE ( 'NONE', *, *, #19425, .T. ) ;
#29872=EDGE_LOOP ( 'NONE', ( #24167, #1600, #21410, #12267 ) ) ;
#29917=FACE_OUTER_BOUND ( 'NONE', #5908, .T. ) ;
#29931=CARTESIAN_POINT ( 'NONE',  ( -9.700000000005733369, -13.84939817521907734, -36.47165854408401486 ) ) ;
#29971=LINE ( 'NONE', #15349, #4215 ) ;
#30162=EDGE_CURVE ( 'NONE', #18133, #7840, #212, .T. ) ;
#30167=CONICAL_SURFACE ( 'NONE', #11085, 0.9999999999991042721, 0.7853981633970000820 ) ;
#30270=PLANE ( 'NONE',  #2919 ) ;
#30384=CARTESIAN_POINT ( 'NONE',  ( 9.799999999987905497, -15.94902145823454198, -35.53273252495090873 ) ) ;
#30851=EDGE_LOOP ( 'NONE', ( #1087, #4568, #10487, #28829, #14398, #29325 ) ) ;
#30858=CARTESIAN_POINT ( 'NONE',  ( -353541.5905939771328, -322767.6580554517568, 144295.1095977958466 ) ) ;
#30878=CARTESIAN_POINT ( 'NONE',  ( -353541.5905929750297, -345962.9896101437625, -72978.28499981865752 ) ) ;
#30921=ORIENTED_EDGE ( 'NONE', *, *, #15083, .T. ) ;
#30977=PLANE ( 'NONE',  #13938 ) ;
#31002=EDGE_CURVE ( 'NONE', #2248, #24939, #25797, .T. ) ;
#31014=CARTESIAN_POINT ( 'NONE',  ( 9.499999999789963567, -17.13335861488235423, -37.56236078282699253 ) ) ;
ENDSEC;
END-ISO-10303-21;
